ISO-10303-21;
HEADER;
FILE_DESCRIPTION (('STEP AP214'),
    '1' );
FILE_NAME ('link.step',
    '2026-10-28T16:30:29',
    ( '' ),
    ( '' ),
    'SwSTEP 2.0',
    'SolidWorks 2025',
    '' );
FILE_SCHEMA (( 'AUTOMOTIVE_DESIGN' ));
ENDSEC;

DATA;
#1=ORIENTED_EDGE ( 'NONE', *, *, #6027, .T. ) ;
#9=EDGE_CURVE ( 'NONE', #2534, #191, #5287, .T. ) ;
#12=DIRECTION ( 'NONE',  ( 1.000000000000000000, 0.000000000000000000, 0.000000000000000000 ) ) ;
#20=EDGE_CURVE ( 'NONE', #1964, #6977, #5721, .T. ) ;
#31=ORIENTED_EDGE ( 'NONE', *, *, #3655, .T. ) ;
#45=AXIS2_PLACEMENT_3D ( 'NONE', #5549, #210, #1347 ) ;
#62=DIRECTION ( 'NONE',  ( 0.000000000000000000, 0.000000000000000000, 1.000000000000000000 ) ) ;
#68=VECTOR ( 'NONE', #7179, 1000.000000000000000 ) ;
#74=DIRECTION ( 'NONE',  ( 0.000000000000000000, 0.000000000000000000, -1.000000000000000000 ) ) ;
#113=DIRECTION ( 'NONE',  ( 5.551115123125785167E-17, -0.7071067811865451302, 0.7071067811865499042 ) ) ;
#116=DIRECTION ( 'NONE',  ( -5.551115123125785167E-17, 0.7071067811865469066, 0.7071067811865482389 ) ) ;
#125=ORIENTED_EDGE ( 'NONE', *, *, #2917, .T. ) ;
#134=CLOSED_SHELL ( 'NONE', ( #4385, #2935, #2103, #5773, #2173, #1411, #598, #7589, #2241, #2766, #3161, #4459, #4149, #7376, #3485, #1798, #883, #2489, #2656, #6564, #2581, #4183, #1712, #6059, #2477, #6043 ) ) ;
#135=VECTOR ( 'NONE', #6601, 1000.000000000000000 ) ;
#136=ORIENTED_EDGE ( 'NONE', *, *, #2636, .T. ) ;
#163=DIRECTION ( 'NONE',  ( 0.000000000000000000, 0.000000000000000000, 1.000000000000000000 ) ) ;
#173=AXIS2_PLACEMENT_3D ( 'NONE', #4766, #2865, #1709 ) ;
#178=CIRCLE ( 'NONE', #1154, 12.49999999999999645 ) ;
#187=AXIS2_PLACEMENT_3D ( 'NONE', #7080, #1809, #2958 ) ;
#191=VERTEX_POINT ( 'NONE', #2258 ) ;
#205=DIRECTION ( 'NONE',  ( 4.622231866529368100E-33, -2.600005424922769496E-32, 1.000000000000000000 ) ) ;
#210=DIRECTION ( 'NONE',  ( -1.000000000000000000, 5.551115123125783935E-17, -4.237045877651919561E-33 ) ) ;
#214=( LENGTH_UNIT ( ) NAMED_UNIT ( * ) SI_UNIT ( .MILLI., .METRE. ) );
#215=CARTESIAN_POINT ( 'NONE',  ( 6.500000000000007994, 12.50000000000001243, 4.999999999999995559 ) ) ;
#223=CARTESIAN_POINT ( 'NONE',  ( 25.00000000000002132, 0.000000000000000000, 4.999999999999992006 ) ) ;
#229=LINE ( 'NONE', #3078, #5734 ) ;
#235=ORIENTED_EDGE ( 'NONE', *, *, #6293, .F. ) ;
#248=AXIS2_PLACEMENT_3D ( 'NONE', #5219, #5144, #2259 ) ;
#251=VECTOR ( 'NONE', #6869, 1000.000000000000000 ) ;
#273=CARTESIAN_POINT ( 'NONE',  ( 24.99999999999999289, 86.00000000000001421, 0.000000000000000000 ) ) ;
#278=ORIENTED_EDGE ( 'NONE', *, *, #2137, .F. ) ;
#281=CARTESIAN_POINT ( 'NONE',  ( 25.00000000000000000, 31.53553390593274841, 6.464466094067257806 ) ) ;
#287=CARTESIAN_POINT ( 'NONE',  ( 0.000000000000000000, 0.000000000000000000, 0.000000000000000000 ) ) ;
#302=( GEOMETRIC_REPRESENTATION_CONTEXT ( 3 ) GLOBAL_UNCERTAINTY_ASSIGNED_CONTEXT ( ( #2943 ) ) GLOBAL_UNIT_ASSIGNED_CONTEXT ( ( #2743, #3947, #5060 ) ) REPRESENTATION_CONTEXT ( 'NONE', 'WORKASPACE' ) );
#303=AXIS2_PLACEMENT_3D ( 'NONE', #887, #7434, #5596 ) ;
#306=CIRCLE ( 'NONE', #4740, 6.000000000000001776 ) ;
#308=VECTOR ( 'NONE', #3550, 1000.000000000000000 ) ;
#315=FACE_OUTER_BOUND ( 'NONE', #5801, .T. ) ;
#328=DIRECTION ( 'NONE',  ( 1.000000000000000000, 0.000000000000000000, 0.000000000000000000 ) ) ;
#337=ORIENTED_EDGE ( 'NONE', *, *, #5469, .T. ) ;
#346=PLANE ( 'NONE',  #6274 ) ;
#356=ORIENTED_EDGE ( 'NONE', *, *, #3273, .T. ) ;
#365=CARTESIAN_POINT ( 'NONE',  ( 25.00000000000000000, 40.21320343559644783, 10.99999999999999467 ) ) ;
#385=CARTESIAN_POINT ( 'NONE',  ( 18.50000000000000711, 101.5000000000000000, -1.214306433183764966E-14 ) ) ;
#403=FACE_BOUND ( 'NONE', #5032, .T. ) ;
#410=CARTESIAN_POINT ( 'NONE',  ( 12.50000000000000355, 101.5000000000000000, 0.000000000000000000 ) ) ;
#413=CIRCLE ( 'NONE', #1764, 6.000000000000001776 ) ;
#414=AXIS2_PLACEMENT_3D ( 'NONE', #6878, #3960, #1027 ) ;
#420=CIRCLE ( 'NONE', #303, 6.000000000000001776 ) ;
#448=FACE_OUTER_BOUND ( 'NONE', #7282, .T. ) ;
#452=VERTEX_POINT ( 'NONE', #7285 ) ;
#457=VECTOR ( 'NONE', #1691, 1000.000000000000000 ) ;
#466=ORIENTED_EDGE ( 'NONE', *, *, #5900, .F. ) ;
#468=ORIENTED_EDGE ( 'NONE', *, *, #3972, .F. ) ;
#472=VERTEX_POINT ( 'NONE', #4991 ) ;
#486=CARTESIAN_POINT ( 'NONE',  ( 25.00000000000000711, 77.32233047033632545, 4.535533905932713772 ) ) ;
#488=CARTESIAN_POINT ( 'NONE',  ( 25.00000000000000711, 40.21320343559642652, 0.9999999999999956701 ) ) ;
#505=VERTEX_POINT ( 'NONE', #822 ) ;
#508=CARTESIAN_POINT ( 'NONE',  ( 24.99999999999999289, 86.00000000000001421, 9.999999999999992895 ) ) ;
#514=DIRECTION ( 'NONE',  ( -1.000000000000000000, 5.551115123125783935E-17, -4.237045877651919561E-33 ) ) ;
#526=CARTESIAN_POINT ( 'NONE',  ( 12.50000000000000355, 101.5000000000000000, -1.214306433183764966E-14 ) ) ;
#527=DIRECTION ( 'NONE',  ( 0.000000000000000000, 0.000000000000000000, 1.000000000000000000 ) ) ;
#531=CARTESIAN_POINT ( 'NONE',  ( 25.00000000000000711, 40.21320343559642652, 0.9999999999999956701 ) ) ;
#553=VECTOR ( 'NONE', #1912, 1000.000000000000000 ) ;
#569=EDGE_LOOP ( 'NONE', ( #5849, #1454, #6085, #6733, #1062, #6851, #7395, #869, #7502, #4960, #1928, #6680, #4753, #4510, #3891, #4894, #31, #7507, #6786, #1205 ) ) ;
#581=EDGE_CURVE ( 'NONE', #2726, #3515, #6939, .T. ) ;
#595=DIRECTION ( 'NONE',  ( 5.551115123125783935E-17, 1.000000000000000000, 5.166928274020107347E-17 ) ) ;
#598=ADVANCED_FACE ( 'NONE', ( #7049 ), #1781, .F. ) ;
#600=DIRECTION ( 'NONE',  ( 4.622231866529368100E-33, -2.600005424922769496E-32, 1.000000000000000000 ) ) ;
#615=DIRECTION ( 'NONE',  ( 5.551115123125782702E-17, -0.7071067811865481278, 0.7071067811865469066 ) ) ;
#631=DIRECTION ( 'NONE',  ( -1.000000000000000000, 5.551115123125783935E-17, -4.237045877651919561E-33 ) ) ;
#642=LINE ( 'NONE', #7218, #2236 ) ;
#648=CARTESIAN_POINT ( 'NONE',  ( 25.00000000000002842, 73.78679656440351664, 11.00000000000000178 ) ) ;
#659=CIRCLE ( 'NONE', #1633, 10.00000000000000178 ) ;
#664=DIRECTION ( 'NONE',  ( 0.000000000000000000, 0.000000000000000000, -1.000000000000000000 ) ) ;
#669=AXIS2_PLACEMENT_3D ( 'NONE', #2903, #631, #1204 ) ;
#697=ORIENTED_EDGE ( 'NONE', *, *, #1070, .T. ) ;
#706=ORIENTED_EDGE ( 'NONE', *, *, #2708, .F. ) ;
#707=DIRECTION ( 'NONE',  ( 5.551115123125783935E-17, 1.000000000000000000, -2.214819436045321778E-32 ) ) ;
#721=ORIENTED_EDGE ( 'NONE', *, *, #3201, .F. ) ;
#725=DIRECTION ( 'NONE',  ( -4.622231866529368100E-33, 2.600005424922769496E-32, -1.000000000000000000 ) ) ;
#728=EDGE_LOOP ( 'NONE', ( #1559, #6181 ) ) ;
#732=DIRECTION ( 'NONE',  ( -1.000000000000000000, 5.551115123125783935E-17, -4.237045877651919561E-33 ) ) ;
#759=CARTESIAN_POINT ( 'NONE',  ( 24.99999999999999289, 86.00000000000001421, 0.000000000000000000 ) ) ;
#760=AXIS2_PLACEMENT_3D ( 'NONE', #488, #6260, #527 ) ;
#766=ORIENTED_EDGE ( 'NONE', *, *, #1949, .T. ) ;
#783=EDGE_LOOP ( 'NONE', ( #3895, #1023, #7436, #4318 ) ) ;
#802=DIRECTION ( 'NONE',  ( 4.622231866529368100E-33, -2.600005424922769496E-32, 1.000000000000000000 ) ) ;
#808=CARTESIAN_POINT ( 'NONE',  ( 12.50000000000001066, 12.50000000000001066, 4.999999999999995559 ) ) ;
#814=AXIS2_PLACEMENT_3D ( 'NONE', #5388, #2457, #3733 ) ;
#818=ORIENTED_EDGE ( 'NONE', *, *, #1594, .F. ) ;
#822=CARTESIAN_POINT ( 'NONE',  ( 1.387778780781445676E-14, 12.49999999999998401, 0.000000000000000000 ) ) ;
#824=VECTOR ( 'NONE', #7054, 999.9999999999998863 ) ;
#829=LINE ( 'NONE', #1950, #3080 ) ;
#839=ORIENTED_EDGE ( 'NONE', *, *, #7076, .T. ) ;
#858=ORIENTED_EDGE ( 'NONE', *, *, #6448, .T. ) ;
#860=DIRECTION ( 'NONE',  ( 1.000000000000000000, -5.551115123125783935E-17, 4.237045877651919561E-33 ) ) ;
#864=LINE ( 'NONE', #5001, #4065 ) ;
#868=VERTEX_POINT ( 'NONE', #385 ) ;
#869=ORIENTED_EDGE ( 'NONE', *, *, #6458, .F. ) ;
#883=ADVANCED_FACE ( 'NONE', ( #2043 ), #346, .F. ) ;
#887=CARTESIAN_POINT ( 'NONE',  ( 12.50000000000000355, 101.5000000000000000, 4.999999999999999112 ) ) ;
#893=EDGE_CURVE ( 'NONE', #6262, #6493, #6660, .T. ) ;
#897=AXIS2_PLACEMENT_3D ( 'NONE', #5217, #1172, #1826 ) ;
#899=FACE_OUTER_BOUND ( 'NONE', #4290, .T. ) ;
#908=VERTEX_POINT ( 'NONE', #5548 ) ;
#914=VECTOR ( 'NONE', #6477, 1000.000000000000000 ) ;
#916=DIRECTION ( 'NONE',  ( -5.551115123125785167E-17, 0.7071067811865452413, -0.7071067811865499042 ) ) ;
#925=DIRECTION ( 'NONE',  ( 4.622231866529368100E-33, -2.600005424922769496E-32, 1.000000000000000000 ) ) ;
#949=EDGE_LOOP ( 'NONE', ( #1449, #5051, #4680, #1723 ) ) ;
#954=DIRECTION ( 'NONE',  ( 1.000000000000000000, 0.000000000000000000, 0.000000000000000000 ) ) ;
#972=ORIENTED_EDGE ( 'NONE', *, *, #7431, .F. ) ;
#993=EDGE_CURVE ( 'NONE', #1663, #6493, #1609, .T. ) ;
#1001=ORIENTED_EDGE ( 'NONE', *, *, #3655, .F. ) ;
#1012=ORIENTED_EDGE ( 'NONE', *, *, #893, .T. ) ;
#1023=ORIENTED_EDGE ( 'NONE', *, *, #7481, .F. ) ;
#1026=DIRECTION ( 'NONE',  ( -5.551115123125785167E-17, 0.7071067811865452413, -0.7071067811865499042 ) ) ;
#1027=DIRECTION ( 'NONE',  ( 1.000000000000000000, 0.000000000000000000, 0.000000000000000000 ) ) ;
#1033=CIRCLE ( 'NONE', #1282, 9.999999999999994671 ) ;
#1039=CARTESIAN_POINT ( 'NONE',  ( 2.775557561562891351E-14, 86.00000000000000000, 4.999999999999999112 ) ) ;
#1056=CARTESIAN_POINT ( 'NONE',  ( 24.99999999999999289, 78.92893218813451028, 2.928932188134522274 ) ) ;
#1062=ORIENTED_EDGE ( 'NONE', *, *, #2200, .F. ) ;
#1070=EDGE_CURVE ( 'NONE', #2618, #4037, #5197, .T. ) ;
#1075=CARTESIAN_POINT ( 'NONE',  ( 24.99999999999998579, 101.4999999999999858, 4.999999999999995559 ) ) ;
#1100=CARTESIAN_POINT ( 'NONE',  ( 2.775557561562891351E-14, 40.21320343559642652, 5.999999999999996447 ) ) ;
#1111=DIRECTION ( 'NONE',  ( -4.622231866529368100E-33, 2.600005424922769496E-32, -1.000000000000000000 ) ) ;
#1116=CARTESIAN_POINT ( 'NONE',  ( 2.775557561562891351E-14, 28.00000000000002487, 9.999999999999992895 ) ) ;
#1119=LINE ( 'NONE', #4591, #1152 ) ;
#1120=LINE ( 'NONE', #3555, #914 ) ;
#1128=VECTOR ( 'NONE', #7412, 1000.000000000000000 ) ;
#1129=DIRECTION ( 'NONE',  ( 0.000000000000000000, 1.000000000000000000, -3.556183125752453755E-15 ) ) ;
#1145=AXIS2_PLACEMENT_3D ( 'NONE', #5159, #925, #3278 ) ;
#1152=VECTOR ( 'NONE', #732, 1000.000000000000000 ) ;
#1154=AXIS2_PLACEMENT_3D ( 'NONE', #410, #6345, #5545 ) ;
#1160=STYLED_ITEM('',(#7624),#6388);
#1171=DIRECTION ( 'NONE',  ( -5.551115123125785167E-17, 0.7071067811865469066, 0.7071067811865482389 ) ) ;
#1172=DIRECTION ( 'NONE',  ( 1.000000000000000000, -5.551115123125783935E-17, 4.237045877651920245E-33 ) ) ;
#1185=CARTESIAN_POINT ( 'NONE',  ( 12.50000000000000355, 101.5000000000000000, 0.000000000000000000 ) ) ;
#1204=DIRECTION ( 'NONE',  ( 0.000000000000000000, 0.000000000000000000, 1.000000000000000000 ) ) ;
#1205=ORIENTED_EDGE ( 'NONE', *, *, #4052, .T. ) ;
#1247=AXIS2_PLACEMENT_3D ( 'NONE', #6677, #5912, #113 ) ;
#1252=AXIS2_PLACEMENT_3D ( 'NONE', #6002, #725, #4854 ) ;
#1262=FACE_OUTER_BOUND ( 'NONE', #6520, .T. ) ;
#1272=CARTESIAN_POINT ( 'NONE',  ( 2.775557561562891351E-14, 40.21320343559642652, 0.9999999999999956701 ) ) ;
#1281=PLANE ( 'NONE',  #6973 ) ;
#1282=AXIS2_PLACEMENT_3D ( 'NONE', #4509, #7464, #2769 ) ;
#1283=CIRCLE ( 'NONE', #669, 4.999999999999999112 ) ;
#1300=ORIENTED_EDGE ( 'NONE', *, *, #9, .T. ) ;
#1301=EDGE_LOOP ( 'NONE', ( #1300, #706, #3023, #6757 ) ) ;
#1302=CARTESIAN_POINT ( 'NONE',  ( 0.000000000000000000, 35.07106781186547551, 2.928932188134524051 ) ) ;
#1322=ORIENTED_EDGE ( 'NONE', *, *, #7568, .T. ) ;
#1329=CARTESIAN_POINT ( 'NONE',  ( 25.00000000000002132, 36.67766952966366745, 4.535533905932717325 ) ) ;
#1344=LINE ( 'NONE', #5476, #5709 ) ;
#1347=DIRECTION ( 'NONE',  ( 0.000000000000000000, 0.000000000000000000, 1.000000000000000000 ) ) ;
#1358=ORIENTED_EDGE ( 'NONE', *, *, #4951, .F. ) ;
#1371=CIRCLE ( 'NONE', #1252, 12.49999999999999645 ) ;
#1377=VERTEX_POINT ( 'NONE', #2987 ) ;
#1389=SHAPE_REPRESENTATION_RELATIONSHIP ( 'NONE' , 'NONE' ,  #6475, #5100 ) ;
#1396=EDGE_CURVE ( 'NONE', #2714, #6636, #7330, .T. ) ;
#1402=PLANE ( 'NONE',  #1247 ) ;
#1403=CARTESIAN_POINT ( 'NONE',  ( 25.00000000000000711, 28.00000000000002487, 4.999999999999995559 ) ) ;
#1408=MECHANICAL_DESIGN_GEOMETRIC_PRESENTATION_REPRESENTATION('',(#1160),#302);
#1411=ADVANCED_FACE ( 'NONE', ( #3873, #5604 ), #6100, .T. ) ;
#1415=CIRCLE ( 'NONE', #1145, 12.49999999999999645 ) ;
#1434=EDGE_CURVE ( 'NONE', #5929, #1595, #3281, .T. ) ;
#1449=ORIENTED_EDGE ( 'NONE', *, *, #4917, .T. ) ;
#1453=CARTESIAN_POINT ( 'NONE',  ( 12.50000000000001066, 12.50000000000001066, -1.214306433183764966E-14 ) ) ;
#1454=ORIENTED_EDGE ( 'NONE', *, *, #6993, .T. ) ;
#1467=AXIS2_PLACEMENT_3D ( 'NONE', #4533, #1513, #6832 ) ;
#1470=CARTESIAN_POINT ( 'NONE',  ( 25.00000000000000000, 12.49999999999998401, 9.999999999999996447 ) ) ;
#1473=CARTESIAN_POINT ( 'NONE',  ( 1.387778780781445676E-14, 73.78679656440351664, 5.999999999999996447 ) ) ;
#1494=VERTEX_POINT ( 'NONE', #1473 ) ;
#1510=CARTESIAN_POINT ( 'NONE',  ( 25.00000000000000000, 40.21320343559644783, 5.999999999999996447 ) ) ;
#1513=DIRECTION ( 'NONE',  ( 1.000000000000000000, -5.551115123125783935E-17, 4.237045877651919561E-33 ) ) ;
#1515=AXIS2_PLACEMENT_3D ( 'NONE', #2286, #5782, #5280 ) ;
#1528=AXIS2_PLACEMENT_3D ( 'NONE', #3603, #3645, #6410 ) ;
#1533=DIRECTION ( 'NONE',  ( 5.551115123125782702E-17, -0.7071067811865481278, 0.7071067811865469066 ) ) ;
#1559=ORIENTED_EDGE ( 'NONE', *, *, #5736, .T. ) ;
#1570=DIRECTION ( 'NONE',  ( -1.000000000000000000, 5.551115123125783935E-17, -4.237045877651919561E-33 ) ) ;
#1594=EDGE_CURVE ( 'NONE', #4747, #2183, #6228, .T. ) ;
#1595=VERTEX_POINT ( 'NONE', #4681 ) ;
#1609=LINE ( 'NONE', #6430, #3203 ) ;
#1621=ORIENTED_EDGE ( 'NONE', *, *, #7168, .F. ) ;
#1633=AXIS2_PLACEMENT_3D ( 'NONE', #7101, #4685, #7022 ) ;
#1656=AXIS2_PLACEMENT_3D ( 'NONE', #4902, #2550, #4399 ) ;
#1663=VERTEX_POINT ( 'NONE', #3946 ) ;
#1667=APPLICATION_CONTEXT ( 'automotive_design' ) ;
#1671=DIRECTION ( 'NONE',  ( 0.000000000000000000, 0.000000000000000000, -1.000000000000000000 ) ) ;
#1676=CARTESIAN_POINT ( 'NONE',  ( 25.00000000000002132, 0.000000000000000000, -1.734723475976807094E-15 ) ) ;
#1681=ORIENTED_EDGE ( 'NONE', *, *, #1594, .T. ) ;
#1683=DIRECTION ( 'NONE',  ( 1.000000000000000000, 0.000000000000000000, 0.000000000000000000 ) ) ;
#1691=DIRECTION ( 'NONE',  ( -1.000000000000000000, 5.551115123125783935E-17, -4.237045877651919561E-33 ) ) ;
#1703=CARTESIAN_POINT ( 'NONE',  ( 25.00000000000002132, 82.46446609406720540, 6.464466094067254254 ) ) ;
#1707=CARTESIAN_POINT ( 'NONE',  ( 2.775557561562891351E-14, 28.00000000000002487, 9.999999999999992895 ) ) ;
#1709=DIRECTION ( 'NONE',  ( 1.000000000000000000, 0.000000000000000000, 0.000000000000000000 ) ) ;
#1712=ADVANCED_FACE ( 'NONE', ( #4721 ), #1281, .T. ) ;
#1717=LINE ( 'NONE', #486, #4363 ) ;
#1723=ORIENTED_EDGE ( 'NONE', *, *, #7327, .T. ) ;
#1727=ORIENTED_EDGE ( 'NONE', *, *, #993, .T. ) ;
#1730=PLANE ( 'NONE',  #4493 ) ;
#1745=DIRECTION ( 'NONE',  ( 1.000000000000000000, -5.551115123125783935E-17, 4.237045877651919561E-33 ) ) ;
#1749=CARTESIAN_POINT ( 'NONE',  ( 0.000000000000000000, 0.000000000000000000, 0.000000000000000000 ) ) ;
#1750=CYLINDRICAL_SURFACE ( 'NONE', #173, 6.000000000000001776 ) ;
#1753=VERTEX_POINT ( 'NONE', #3642 ) ;
#1757=CARTESIAN_POINT ( 'NONE',  ( 2.775557561562891351E-14, 86.00000000000000000, 9.999999999999996447 ) ) ;
#1764=AXIS2_PLACEMENT_3D ( 'NONE', #6046, #5972, #7199 ) ;
#1766=AXIS2_PLACEMENT_3D ( 'NONE', #6337, #3949, #6290 ) ;
#1776=DIRECTION ( 'NONE',  ( 5.551115123125783935E-17, 1.000000000000000000, -2.214819436045321778E-32 ) ) ;
#1781=CYLINDRICAL_SURFACE ( 'NONE', #5295, 5.000000000000009770 ) ;
#1787=CARTESIAN_POINT ( 'NONE',  ( 25.00000000000001421, 35.07106781186547551, 2.928932188134525827 ) ) ;
#1794=PRODUCT_DEFINITION_CONTEXT ( 'detailed design', #1667, 'design' ) ;
#1795=ORIENTED_EDGE ( 'NONE', *, *, #3731, .T. ) ;
#1798=ADVANCED_FACE ( 'NONE', ( #3024 ), #7099, .T. ) ;
#1807=CARTESIAN_POINT ( 'NONE',  ( 25.00000000000000711, 40.21320343559642652, 10.99999999999999467 ) ) ;
#1809=DIRECTION ( 'NONE',  ( 1.000000000000000000, -5.551115123125783935E-17, 4.237045877651919561E-33 ) ) ;
#1810=ORIENTED_EDGE ( 'NONE', *, *, #5263, .T. ) ;
#1826=DIRECTION ( 'NONE',  ( 5.551115123125783935E-17, 1.000000000000000000, -2.214819436045321778E-32 ) ) ;
#1836=EDGE_CURVE ( 'NONE', #2926, #908, #4288, .T. ) ;
#1852=LINE ( 'NONE', #4208, #2877 ) ;
#1864=DIRECTION ( 'NONE',  ( 1.000000000000000000, 0.000000000000000000, 0.000000000000000000 ) ) ;
#1899=DIRECTION ( 'NONE',  ( -4.622231866529368100E-33, 2.600005424922769496E-32, -1.000000000000000000 ) ) ;
#1902=DIRECTION ( 'NONE',  ( -6.162975822039153361E-33, -5.166928274020107963E-17, 1.000000000000000000 ) ) ;
#1905=EDGE_CURVE ( 'NONE', #5154, #6636, #7350, .T. ) ;
#1912=DIRECTION ( 'NONE',  ( -1.000000000000000000, 5.551115123125783935E-17, -4.237045877651919561E-33 ) ) ;
#1914=AXIS2_PLACEMENT_3D ( 'NONE', #1749, #62, #1864 ) ;
#1928=ORIENTED_EDGE ( 'NONE', *, *, #5003, .F. ) ;
#1934=CARTESIAN_POINT ( 'NONE',  ( 6.500000000000000888, 101.5000000000000000, 4.999999999999999112 ) ) ;
#1940=VERTEX_POINT ( 'NONE', #4905 ) ;
#1949=EDGE_CURVE ( 'NONE', #3811, #2040, #2620, .T. ) ;
#1950=CARTESIAN_POINT ( 'NONE',  ( 18.50000000000000711, 101.5000000000000000, -1.214306433183764966E-14 ) ) ;
#1964=VERTEX_POINT ( 'NONE', #1807 ) ;
#1977=EDGE_CURVE ( 'NONE', #6977, #452, #5921, .T. ) ;
#1978=CARTESIAN_POINT ( 'NONE',  ( 24.99999999999999289, 86.00000000000001421, 4.999999999999992006 ) ) ;
#1990=DIRECTION ( 'NONE',  ( -4.237045877651920929E-33, -1.945189243831109306E-32, 1.000000000000000000 ) ) ;
#2003=ORIENTED_EDGE ( 'NONE', *, *, #3395, .F. ) ;
#2006=ORIENTED_EDGE ( 'NONE', *, *, #3422, .F. ) ;
#2024=DIRECTION ( 'NONE',  ( -1.000000000000000000, 5.551115123125783935E-17, -4.237045877651919561E-33 ) ) ;
#2030=VECTOR ( 'NONE', #3418, 1000.000000000000000 ) ;
#2036=CARTESIAN_POINT ( 'NONE',  ( 24.99999999999998579, 101.4999999999999858, -1.734723475976807094E-15 ) ) ;
#2037=LINE ( 'NONE', #6143, #2365 ) ;
#2040=VERTEX_POINT ( 'NONE', #1075 ) ;
#2043=FACE_OUTER_BOUND ( 'NONE', #5010, .T. ) ;
#2051=AXIS2_PLACEMENT_3D ( 'NONE', #1707, #1745, #1671 ) ;
#2057=ORIENTED_EDGE ( 'NONE', *, *, #7168, .T. ) ;
#2058=AXIS2_PLACEMENT_3D ( 'NONE', #531, #6427, #4628 ) ;
#2068=ORIENTED_EDGE ( 'NONE', *, *, #3483, .T. ) ;
#2073=EDGE_CURVE ( 'NONE', #908, #472, #2429, .T. ) ;
#2077=ORIENTED_EDGE ( 'NONE', *, *, #6933, .T. ) ;
#2103=ADVANCED_FACE ( 'NONE', ( #2277 ), #5852, .T. ) ;
#2116=VERTEX_POINT ( 'NONE', #3770 ) ;
#2117=DIRECTION ( 'NONE',  ( -5.551115123125785167E-17, 0.7071067811865469066, 0.7071067811865482389 ) ) ;
#2130=AXIS2_PLACEMENT_3D ( 'NONE', #1116, #5198, #4127 ) ;
#2137=EDGE_CURVE ( 'NONE', #6069, #1494, #6110, .T. ) ;
#2146=AXIS2_PLACEMENT_3D ( 'NONE', #808, #205, #3159 ) ;
#2148=FACE_OUTER_BOUND ( 'NONE', #5700, .T. ) ;
#2153=ORIENTED_EDGE ( 'NONE', *, *, #3745, .F. ) ;
#2173=ADVANCED_FACE ( 'NONE', ( #7191, #3042 ), #7116, .F. ) ;
#2183=VERTEX_POINT ( 'NONE', #1302 ) ;
#2188=LINE ( 'NONE', #4540, #7065 ) ;
#2200=EDGE_CURVE ( 'NONE', #5737, #2726, #229, .T. ) ;
#2206=DIRECTION ( 'NONE',  ( -1.000000000000000000, 5.551115123125783935E-17, -4.237045877651919561E-33 ) ) ;
#2209=ORIENTED_EDGE ( 'NONE', *, *, #1070, .F. ) ;
#2214=DIRECTION ( 'NONE',  ( -1.000000000000000000, 5.551115123125783935E-17, -4.237045877651919561E-33 ) ) ;
#2224=ORIENTED_EDGE ( 'NONE', *, *, #6620, .F. ) ;
#2235=DIRECTION ( 'NONE',  ( 4.622231866529368100E-33, -2.600005424922769496E-32, 1.000000000000000000 ) ) ;
#2236=VECTOR ( 'NONE', #4298, 1000.000000000000114 ) ;
#2241=ADVANCED_FACE ( 'NONE', ( #1262 ), #3620, .T. ) ;
#2251=DIRECTION ( 'NONE',  ( 4.622231866529368100E-33, -2.600005424922769496E-32, 1.000000000000000000 ) ) ;
#2258=CARTESIAN_POINT ( 'NONE',  ( 2.775557561562891351E-14, 86.00000000000000000, -1.387778780781445676E-14 ) ) ;
#2259=DIRECTION ( 'NONE',  ( 1.000000000000000000, 0.000000000000000000, 0.000000000000000000 ) ) ;
#2277=FACE_OUTER_BOUND ( 'NONE', #4409, .T. ) ;
#2286=CARTESIAN_POINT ( 'NONE',  ( 25.00000000000002132, 73.78679656440357348, 0.9999999999999991118 ) ) ;
#2289=ORIENTED_EDGE ( 'NONE', *, *, #5955, .T. ) ;
#2305=DIRECTION ( 'NONE',  ( 0.000000000000000000, 1.000000000000000000, -1.617781153285278938E-32 ) ) ;
#2316=DIRECTION ( 'NONE',  ( 5.551115123125783935E-17, -0.7071067811865469066, -0.7071067811865481278 ) ) ;
#2334=VECTOR ( 'NONE', #3683, 1000.000000000000000 ) ;
#2362=ORIENTED_EDGE ( 'NONE', *, *, #2533, .F. ) ;
#2365=VECTOR ( 'NONE', #916, 1000.000000000000114 ) ;
#2387=LINE ( 'NONE', #7578, #308 ) ;
#2400=FACE_OUTER_BOUND ( 'NONE', #5121, .T. ) ;
#2404=CARTESIAN_POINT ( 'NONE',  ( 25.00000000000002132, 73.78679656440357348, 0.9999999999999991118 ) ) ;
#2413=CARTESIAN_POINT ( 'NONE',  ( 3.469446951953614189E-14, 80.85786437626907741, 8.071067811865438202 ) ) ;
#2429=CIRCLE ( 'NONE', #2058, 4.999999999999999112 ) ;
#2441=CARTESIAN_POINT ( 'NONE',  ( 25.00000000000000711, 28.00000000000002487, 9.999999999999996447 ) ) ;
#2457=DIRECTION ( 'NONE',  ( -1.000000000000000000, 5.551115123125783935E-17, -4.237045877651919561E-33 ) ) ;
#2473=CARTESIAN_POINT ( 'NONE',  ( 24.99999999999999289, 86.00000000000001421, 9.999999999999992895 ) ) ;
#2474=CARTESIAN_POINT ( 'NONE',  ( 18.50000000000001421, 12.50000000000001066, 4.999999999999995559 ) ) ;
#2477=ADVANCED_FACE ( 'NONE', ( #4616 ), #4073, .F. ) ;
#2484=DIRECTION ( 'NONE',  ( 5.551115123125790098E-17, 1.000000000000000000, -8.890457814381140303E-16 ) ) ;
#2489=ADVANCED_FACE ( 'NONE', ( #4731 ), #2911, .F. ) ;
#2518=LINE ( 'NONE', #3062, #7428 ) ;
#2523=LINE ( 'NONE', #1470, #2334 ) ;
#2533=EDGE_CURVE ( 'NONE', #2116, #2534, #642, .T. ) ;
#2534=VERTEX_POINT ( 'NONE', #4842 ) ;
#2548=ORIENTED_EDGE ( 'NONE', *, *, #4878, .F. ) ;
#2550=DIRECTION ( 'NONE',  ( -1.000000000000000000, 5.551115123125783935E-17, -4.237045877651919561E-33 ) ) ;
#2556=LINE ( 'NONE', #3098, #4823 ) ;
#2561=CARTESIAN_POINT ( 'NONE',  ( 25.00000000000001421, 35.07106781186547551, 2.928932188134525827 ) ) ;
#2581=ADVANCED_FACE ( 'NONE', ( #4336 ), #1402, .F. ) ;
#2583=VERTEX_POINT ( 'NONE', #2413 ) ;
#2610=ORIENTED_EDGE ( 'NONE', *, *, #6448, .F. ) ;
#2618=VERTEX_POINT ( 'NONE', #4529 ) ;
#2620=LINE ( 'NONE', #4982, #3415 ) ;
#2628=AXIS2_PLACEMENT_3D ( 'NONE', #4380, #5491, #2484 ) ;
#2632=EDGE_LOOP ( 'NONE', ( #3459, #4988, #6672, #7530 ) ) ;
#2636=EDGE_CURVE ( 'NONE', #2722, #1494, #7363, .T. ) ;
#2653=ORIENTED_EDGE ( 'NONE', *, *, #6027, .F. ) ;
#2655=CARTESIAN_POINT ( 'NONE',  ( 12.50000000000000355, 101.5000000000000000, -1.214306433183764966E-14 ) ) ;
#2656=ADVANCED_FACE ( 'NONE', ( #899 ), #6790, .F. ) ;
#2673=CARTESIAN_POINT ( 'NONE',  ( 1.387778780781445676E-14, 12.49999999999998401, 4.999999999999999112 ) ) ;
#2705=ORIENTED_EDGE ( 'NONE', *, *, #7577, .T. ) ;
#2707=DIRECTION ( 'NONE',  ( 4.622231866529368100E-33, -2.600005424922769496E-32, 1.000000000000000000 ) ) ;
#2708=EDGE_CURVE ( 'NONE', #7449, #191, #2556, .T. ) ;
#2714=VERTEX_POINT ( 'NONE', #215 ) ;
#2722=VERTEX_POINT ( 'NONE', #5985 ) ;
#2725=EDGE_CURVE ( 'NONE', #505, #7420, #3792, .T. ) ;
#2726=VERTEX_POINT ( 'NONE', #3065 ) ;
#2736=DIRECTION ( 'NONE',  ( 1.000000000000000000, 0.000000000000000000, 0.000000000000000000 ) ) ;
#2742=CIRCLE ( 'NONE', #1766, 6.000000000000001776 ) ;
#2743=( LENGTH_UNIT ( ) NAMED_UNIT ( * ) SI_UNIT ( .MILLI., .METRE. ) );
#2744=DIRECTION ( 'NONE',  ( -5.551115123125783935E-17, -1.000000000000000000, -5.166928274020107963E-17 ) ) ;
#2746=AXIS2_PLACEMENT_3D ( 'NONE', #3480, #7050, #12 ) ;
#2766=ADVANCED_FACE ( 'NONE', ( #6097 ), #7171, .T. ) ;
#2769=DIRECTION ( 'NONE',  ( 0.000000000000000000, 1.000000000000000000, -6.223320470066798607E-15 ) ) ;
#2794=AXIS2_PLACEMENT_3D ( 'NONE', #2441, #6559, #5443 ) ;
#2819=CARTESIAN_POINT ( 'NONE',  ( 24.99999999999999289, 86.00000000000001421, 9.999999999999992895 ) ) ;
#2825=VECTOR ( 'NONE', #595, 1000.000000000000000 ) ;
#2855=ORIENTED_EDGE ( 'NONE', *, *, #3972, .T. ) ;
#2865=DIRECTION ( 'NONE',  ( 4.622231866529368100E-33, -2.600005424922769496E-32, 1.000000000000000000 ) ) ;
#2870=EDGE_CURVE ( 'NONE', #1753, #505, #1371, .T. ) ;
#2877=VECTOR ( 'NONE', #1776, 1000.000000000000000 ) ;
#2903=CARTESIAN_POINT ( 'NONE',  ( 6.938893903907228378E-15, 73.78679656440351664, 0.9999999999999991118 ) ) ;
#2911=CYLINDRICAL_SURFACE ( 'NONE', #4387, 4.999999999999999112 ) ;
#2917=EDGE_CURVE ( 'NONE', #2583, #3515, #2037, .T. ) ;
#2918=ORIENTED_EDGE ( 'NONE', *, *, #5003, .T. ) ;
#2925=CARTESIAN_POINT ( 'NONE',  ( 25.00000000000002132, 28.00000000000002487, 0.000000000000000000 ) ) ;
#2926=VERTEX_POINT ( 'NONE', #4391 ) ;
#2935=ADVANCED_FACE ( 'NONE', ( #5616 ), #5538, .F. ) ;
#2940=FACE_OUTER_BOUND ( 'NONE', #4142, .T. ) ;
#2943=UNCERTAINTY_MEASURE_WITH_UNIT (LENGTH_MEASURE( 1.000000000000000082E-05 ), #2743, 'distance_accuracy_value', 'NONE');
#2958=DIRECTION ( 'NONE',  ( 0.000000000000000000, 1.000000000000000000, 0.000000000000000000 ) ) ;
#2967=VECTOR ( 'NONE', #6829, 1000.000000000000000 ) ;
#2977=DIRECTION ( 'NONE',  ( 1.000000000000000000, -5.551115123125783935E-17, 4.237045877651920245E-33 ) ) ;
#2986=AXIS2_PLACEMENT_3D ( 'NONE', #6326, #2251, #2736 ) ;
#2987=CARTESIAN_POINT ( 'NONE',  ( 6.500000000000007994, 12.50000000000001243, -1.214306433183764966E-14 ) ) ;
#2990=CARTESIAN_POINT ( 'NONE',  ( 25.00000000000000711, 28.00000000000002487, 9.999999999999996447 ) ) ;
#2991=LINE ( 'NONE', #7033, #3719 ) ;
#2992=EDGE_CURVE ( 'NONE', #5355, #4160, #3735, .T. ) ;
#2996=ORIENTED_EDGE ( 'NONE', *, *, #3731, .F. ) ;
#3000=ORIENTED_EDGE ( 'NONE', *, *, #5809, .F. ) ;
#3007=CIRCLE ( 'NONE', #2146, 6.000000000000001776 ) ;
#3011=DIRECTION ( 'NONE',  ( -1.000000000000000000, 5.551115123125783935E-17, -4.237045877651919561E-33 ) ) ;
#3017=VECTOR ( 'NONE', #1171, 999.9999999999998863 ) ;
#3023=ORIENTED_EDGE ( 'NONE', *, *, #4052, .F. ) ;
#3024=FACE_OUTER_BOUND ( 'NONE', #3717, .T. ) ;
#3036=LINE ( 'NONE', #5383, #5042 ) ;
#3042=FACE_OUTER_BOUND ( 'NONE', #7596, .T. ) ;
#3053=EDGE_CURVE ( 'NONE', #191, #6725, #5119, .T. ) ;
#3062=CARTESIAN_POINT ( 'NONE',  ( 1.387778780781445676E-14, 101.5000000000000000, -1.734723475976807094E-15 ) ) ;
#3065=CARTESIAN_POINT ( 'NONE',  ( 25.00000000000002132, 82.46446609406720540, 6.464466094067254254 ) ) ;
#3072=DIRECTION ( 'NONE',  ( -1.000000000000000000, 5.551115123125783935E-17, -4.237045877651919561E-33 ) ) ;
#3078=CARTESIAN_POINT ( 'NONE',  ( 25.00000000000001421, 80.85786437626907741, 8.071067811865434649 ) ) ;
#3080=VECTOR ( 'NONE', #4301, 1000.000000000000000 ) ;
#3087=EDGE_LOOP ( 'NONE', ( #3000, #4896, #337, #3473 ) ) ;
#3093=EDGE_LOOP ( 'NONE', ( #858, #4496, #3358, #136 ) ) ;
#3098=CARTESIAN_POINT ( 'NONE',  ( 24.99999999999999289, 86.00000000000001421, -1.214306433183764966E-14 ) ) ;
#3103=CARTESIAN_POINT ( 'NONE',  ( 12.50000000000001066, 12.50000000000001066, 4.999999999999995559 ) ) ;
#3111=DIRECTION ( 'NONE',  ( -5.551115123125785167E-17, 0.7071067811865452413, -0.7071067811865499042 ) ) ;
#3159=DIRECTION ( 'NONE',  ( 1.000000000000000000, 0.000000000000000000, 0.000000000000000000 ) ) ;
#3161=ADVANCED_FACE ( 'NONE', ( #4579 ), #5073, .T. ) ;
#3183=ORIENTED_EDGE ( 'NONE', *, *, #7228, .F. ) ;
#3185=DIRECTION ( 'NONE',  ( 1.000000000000000000, -5.551115123125783935E-17, 4.237045877651919561E-33 ) ) ;
#3201=EDGE_CURVE ( 'NONE', #5278, #452, #2991, .T. ) ;
#3203=VECTOR ( 'NONE', #1570, 1000.000000000000000 ) ;
#3210=PRODUCT ( 'link', 'link', '', ( #4757 ) ) ;
#3216=CARTESIAN_POINT ( 'NONE',  ( 25.00000000000000000, 73.78679656440354506, 5.999999999999996447 ) ) ;
#3221=DIRECTION ( 'NONE',  ( -1.000000000000000000, 5.551115123125783935E-17, -4.237045877651919561E-33 ) ) ;
#3234=CARTESIAN_POINT ( 'NONE',  ( 18.50000000000001421, 12.50000000000001066, -1.214306433183764966E-14 ) ) ;
#3254=ORIENTED_EDGE ( 'NONE', *, *, #4324, .T. ) ;
#3261=ORIENTED_EDGE ( 'NONE', *, *, #7337, .F. ) ;
#3273=EDGE_CURVE ( 'NONE', #1595, #1663, #3036, .T. ) ;
#3278=DIRECTION ( 'NONE',  ( 1.000000000000000000, 0.000000000000000000, 0.000000000000000000 ) ) ;
#3281=CIRCLE ( 'NONE', #5250, 5.000000000000004441 ) ;
#3358=ORIENTED_EDGE ( 'NONE', *, *, #4832, .F. ) ;
#3380=VECTOR ( 'NONE', #2305, 1000.000000000000000 ) ;
#3389=CIRCLE ( 'NONE', #7303, 10.00000000000000178 ) ;
#3395=EDGE_CURVE ( 'NONE', #1377, #2714, #4920, .T. ) ;
#3402=AXIS2_PLACEMENT_3D ( 'NONE', #6958, #600, #1683 ) ;
#3409=DIRECTION ( 'NONE',  ( -1.000000000000000000, 5.551115123125783935E-17, -4.237045877651919561E-33 ) ) ;
#3415=VECTOR ( 'NONE', #7319, 1000.000000000000000 ) ;
#3418=DIRECTION ( 'NONE',  ( -1.000000000000000000, 5.551115123125783935E-17, -4.237045877651919561E-33 ) ) ;
#3422=EDGE_CURVE ( 'NONE', #868, #1940, #829, .T. ) ;
#3439=EDGE_CURVE ( 'NONE', #5727, #2116, #864, .T. ) ;
#3443=ORIENTED_EDGE ( 'NONE', *, *, #6405, .T. ) ;
#3459=ORIENTED_EDGE ( 'NONE', *, *, #2992, .F. ) ;
#3461=DIRECTION ( 'NONE',  ( -1.000000000000000000, 5.551115123125783935E-17, -4.237045877651919561E-33 ) ) ;
#3473=ORIENTED_EDGE ( 'NONE', *, *, #7228, .T. ) ;
#3480=CARTESIAN_POINT ( 'NONE',  ( 12.50000000000000355, 101.5000000000000000, -1.214306433183764966E-14 ) ) ;
#3483=EDGE_CURVE ( 'NONE', #1377, #5154, #6999, .T. ) ;
#3485=ADVANCED_FACE ( 'NONE', ( #403, #448 ), #5760, .F. ) ;
#3502=ORIENTED_EDGE ( 'NONE', *, *, #9, .F. ) ;
#3515=VERTEX_POINT ( 'NONE', #4534 ) ;
#3550=DIRECTION ( 'NONE',  ( 5.551115123125783935E-17, 1.000000000000000000, -2.214819436045321778E-32 ) ) ;
#3551=ORIENTED_EDGE ( 'NONE', *, *, #6933, .F. ) ;
#3555=CARTESIAN_POINT ( 'NONE',  ( 0.000000000000000000, 0.000000000000000000, 4.999999999999999112 ) ) ;
#3577=VECTOR ( 'NONE', #6106, 1000.000000000000000 ) ;
#3602=CYLINDRICAL_SURFACE ( 'NONE', #5350, 4.999999999999999112 ) ;
#3603=CARTESIAN_POINT ( 'NONE',  ( 25.00000000000001421, 80.85786437626907741, 8.071067811865434649 ) ) ;
#3619=ORIENTED_EDGE ( 'NONE', *, *, #6866, .F. ) ;
#3620=CYLINDRICAL_SURFACE ( 'NONE', #814, 9.999999999999996447 ) ;
#3628=CIRCLE ( 'NONE', #187, 5.000000000000004441 ) ;
#3629=VECTOR ( 'NONE', #2214, 1000.000000000000000 ) ;
#3642=CARTESIAN_POINT ( 'NONE',  ( 25.00000000000000000, 12.49999999999998401, 0.000000000000000000 ) ) ;
#3645=DIRECTION ( 'NONE',  ( 5.551115123125783935E-17, 0.7071067811865499042, 0.7071067811865451302 ) ) ;
#3655=EDGE_CURVE ( 'NONE', #472, #2722, #5874, .T. ) ;
#3661=DIRECTION ( 'NONE',  ( 5.551115123125783935E-17, 1.000000000000000000, 5.166928274020107347E-17 ) ) ;
#3683=DIRECTION ( 'NONE',  ( -4.622231866529368100E-33, 2.600005424922769496E-32, -1.000000000000000000 ) ) ;
#3691=AXIS2_PLACEMENT_3D ( 'NONE', #1676, #6952, #6377 ) ;
#3701=EDGE_LOOP ( 'NONE', ( #2653, #5014, #7487, #6306 ) ) ;
#3706=ORIENTED_EDGE ( 'NONE', *, *, #3201, .T. ) ;
#3710=ORIENTED_EDGE ( 'NONE', *, *, #4429, .F. ) ;
#3713=DIRECTION ( 'NONE',  ( -1.000000000000000000, 5.551115123125783935E-17, -4.237045877651919561E-33 ) ) ;
#3717=EDGE_LOOP ( 'NONE', ( #1681, #3261, #466, #3443 ) ) ;
#3719=VECTOR ( 'NONE', #5301, 1000.000000000000000 ) ;
#3726=FACE_OUTER_BOUND ( 'NONE', #5882, .T. ) ;
#3731=EDGE_CURVE ( 'NONE', #505, #4747, #6746, .T. ) ;
#3733=DIRECTION ( 'NONE',  ( 0.000000000000000000, 0.000000000000000000, 1.000000000000000000 ) ) ;
#3735=LINE ( 'NONE', #6076, #6161 ) ;
#3740=AXIS2_PLACEMENT_3D ( 'NONE', #1272, #3011, #163 ) ;
#3741=AXIS2_PLACEMENT_3D ( 'NONE', #1757, #5845, #4775 ) ;
#3745=EDGE_CURVE ( 'NONE', #5285, #1753, #2523, .T. ) ;
#3770=CARTESIAN_POINT ( 'NONE',  ( 1.387778780781445676E-14, 77.32233047033629703, 4.535533905932708443 ) ) ;
#3771=CARTESIAN_POINT ( 'NONE',  ( 24.99999999999999289, 78.92893218813451028, 2.928932188134522274 ) ) ;
#3792=LINE ( 'NONE', #4328, #5434 ) ;
#3800=LINE ( 'NONE', #2561, #7553 ) ;
#3811=VERTEX_POINT ( 'NONE', #1978 ) ;
#3817=DIRECTION ( 'NONE',  ( 5.551115123125783935E-17, -0.7071067811865469066, -0.7071067811865481278 ) ) ;
#3852=CIRCLE ( 'NONE', #4720, 10.00000000000000711 ) ;
#3869=ORIENTED_EDGE ( 'NONE', *, *, #1836, .F. ) ;
#3873=FACE_BOUND ( 'NONE', #5971, .T. ) ;
#3891=ORIENTED_EDGE ( 'NONE', *, *, #1836, .T. ) ;
#3895=ORIENTED_EDGE ( 'NONE', *, *, #2533, .T. ) ;
#3927=CARTESIAN_POINT ( 'NONE',  ( 2.775557561562891351E-14, 40.21320343559642652, 10.99999999999999467 ) ) ;
#3946=CARTESIAN_POINT ( 'NONE',  ( 25.00000000000002842, 33.14213562373094391, 8.071067811865434649 ) ) ;
#3947=( NAMED_UNIT ( * ) PLANE_ANGLE_UNIT ( ) SI_UNIT ( $, .RADIAN. ) );
#3949=DIRECTION ( 'NONE',  ( 4.622231866529368100E-33, -2.600005424922769496E-32, 1.000000000000000000 ) ) ;
#3952=VECTOR ( 'NONE', #2117, 999.9999999999998863 ) ;
#3956=EDGE_LOOP ( 'NONE', ( #766, #3254, #2209, #3183 ) ) ;
#3960=DIRECTION ( 'NONE',  ( 4.622231866529368100E-33, -2.600005424922769496E-32, 1.000000000000000000 ) ) ;
#3965=ORIENTED_EDGE ( 'NONE', *, *, #2870, .T. ) ;
#3972=EDGE_CURVE ( 'NONE', #7420, #5285, #6923, .T. ) ;
#4010=EDGE_LOOP ( 'NONE', ( #2003, #6511, #6350, #6238 ) ) ;
#4024=AXIS2_PLACEMENT_3D ( 'NONE', #3103, #2707, #328 ) ;
#4026=ORIENTED_EDGE ( 'NONE', *, *, #3483, .F. ) ;
#4036=APPLICATION_CONTEXT ( 'automotive_design' ) ;
#4037=VERTEX_POINT ( 'NONE', #5897 ) ;
#4052=EDGE_CURVE ( 'NONE', #5611, #7449, #3852, .T. ) ;
#4053=ORIENTED_EDGE ( 'NONE', *, *, #7431, .T. ) ;
#4056=ORIENTED_EDGE ( 'NONE', *, *, #2917, .F. ) ;
#4060=ORIENTED_EDGE ( 'NONE', *, *, #4917, .F. ) ;
#4065=VECTOR ( 'NONE', #3221, 1000.000000000000000 ) ;
#4073=CYLINDRICAL_SURFACE ( 'NONE', #3402, 6.000000000000001776 ) ;
#4087=ORIENTED_EDGE ( 'NONE', *, *, #4117, .F. ) ;
#4117=EDGE_CURVE ( 'NONE', #5355, #868, #7406, .T. ) ;
#4121=AXIS2_PLACEMENT_3D ( 'NONE', #223, #4299, #6064 ) ;
#4127=DIRECTION ( 'NONE',  ( 5.551115123125782702E-17, 1.000000000000000000, 0.000000000000000000 ) ) ;
#4142=EDGE_LOOP ( 'NONE', ( #697, #5868, #4857, #3502, #2362, #2610, #278, #4060, #4782, #818, #2996, #5891, #2077, #5617, #1012, #1, #3706, #7185, #125, #5333 ) ) ;
#4143=AXIS2_PLACEMENT_3D ( 'NONE', #759, #1990, #3185 ) ;
#4149=ADVANCED_FACE ( 'NONE', ( #2400 ), #4759, .F. ) ;
#4154=DIRECTION ( 'NONE',  ( 0.000000000000000000, 0.000000000000000000, 1.000000000000000000 ) ) ;
#4160=VERTEX_POINT ( 'NONE', #1934 ) ;
#4168=ORIENTED_EDGE ( 'NONE', *, *, #7107, .F. ) ;
#4180=CARTESIAN_POINT ( 'NONE',  ( 25.00000000000000711, 40.21320343559642652, 0.9999999999999956701 ) ) ;
#4181=ORIENTED_EDGE ( 'NONE', *, *, #4532, .F. ) ;
#4183=ADVANCED_FACE ( 'NONE', ( #6702 ), #6626, .T. ) ;
#4208=CARTESIAN_POINT ( 'NONE',  ( 25.00000000000002132, 0.000000000000000000, 4.999999999999992006 ) ) ;
#4219=LINE ( 'NONE', #5255, #3017 ) ;
#4288=LINE ( 'NONE', #1787, #824 ) ;
#4290=EDGE_LOOP ( 'NONE', ( #7028, #5114, #1001, #2705 ) ) ;
#4298=DIRECTION ( 'NONE',  ( -5.551115123125785167E-17, 0.7071067811865452413, -0.7071067811865499042 ) ) ;
#4299=DIRECTION ( 'NONE',  ( -4.237045877651920929E-33, -2.600005424922769496E-32, 1.000000000000000000 ) ) ;
#4301=DIRECTION ( 'NONE',  ( 4.622231866529368100E-33, -2.600005424922769496E-32, 1.000000000000000000 ) ) ;
#4318=ORIENTED_EDGE ( 'NONE', *, *, #3439, .T. ) ;
#4324=EDGE_CURVE ( 'NONE', #2040, #4037, #1415, .T. ) ;
#4325=LINE ( 'NONE', #281, #4480 ) ;
#4328=CARTESIAN_POINT ( 'NONE',  ( 1.387778780781445676E-14, 12.49999999999998401, 4.999999999999999112 ) ) ;
#4333=DIRECTION ( 'NONE',  ( 0.000000000000000000, 1.000000000000000000, 0.000000000000000000 ) ) ;
#4336=FACE_OUTER_BOUND ( 'NONE', #783, .T. ) ;
#4348=AXIS2_PLACEMENT_3D ( 'NONE', #2990, #7032, #74 ) ;
#4363=VECTOR ( 'NONE', #1026, 1000.000000000000114 ) ;
#4380=CARTESIAN_POINT ( 'NONE',  ( 6.938893903907228378E-15, 73.78679656440351664, 0.9999999999999991118 ) ) ;
#4385=ADVANCED_FACE ( 'NONE', ( #315 ), #5081, .F. ) ;
#4387=AXIS2_PLACEMENT_3D ( 'NONE', #6382, #3461, #4154 ) ;
#4391=CARTESIAN_POINT ( 'NONE',  ( 25.00000000000001421, 35.07106781186547551, 2.928932188134525827 ) ) ;
#4399=DIRECTION ( 'NONE',  ( 0.000000000000000000, 0.000000000000000000, 1.000000000000000000 ) ) ;
#4409=EDGE_LOOP ( 'NONE', ( #5711, #6646, #2224, #6835 ) ) ;
#4418=EDGE_LOOP ( 'NONE', ( #721, #2548, #4778, #7407 ) ) ;
#4429=EDGE_CURVE ( 'NONE', #5303, #6262, #5458, .T. ) ;
#4431=CARTESIAN_POINT ( 'NONE',  ( 1.387778780781445676E-14, 31.53553390593269512, 6.464466094067257806 ) ) ;
#4443=VERTEX_POINT ( 'NONE', #2925 ) ;
#4459=ADVANCED_FACE ( 'NONE', ( #5277 ), #1730, .T. ) ;
#4480=VECTOR ( 'NONE', #3713, 1000.000000000000000 ) ;
#4487=DIRECTION ( 'NONE',  ( 1.000000000000000000, -5.551115123125783935E-17, 4.237045877651919561E-33 ) ) ;
#4493=AXIS2_PLACEMENT_3D ( 'NONE', #5311, #615, #2316 ) ;
#4496=ORIENTED_EDGE ( 'NONE', *, *, #3439, .F. ) ;
#4503=CYLINDRICAL_SURFACE ( 'NONE', #414, 12.49999999999999645 ) ;
#4509=CARTESIAN_POINT ( 'NONE',  ( 25.00000000000002132, 73.78679656440357348, 0.9999999999999991118 ) ) ;
#4510=ORIENTED_EDGE ( 'NONE', *, *, #5900, .T. ) ;
#4526=ORIENTED_EDGE ( 'NONE', *, *, #2992, .T. ) ;
#4529=CARTESIAN_POINT ( 'NONE',  ( 2.775557561562891351E-14, 86.00000000000000000, 4.999999999999999112 ) ) ;
#4530=LINE ( 'NONE', #1056, #2030 ) ;
#4532=EDGE_CURVE ( 'NONE', #1753, #4443, #2387, .T. ) ;
#4533=CARTESIAN_POINT ( 'NONE',  ( 2.775557561562891351E-14, 86.00000000000000000, 9.999999999999996447 ) ) ;
#4534=CARTESIAN_POINT ( 'NONE',  ( 2.775557561562891351E-14, 82.46446609406723383, 6.464466094067257806 ) ) ;
#4540=CARTESIAN_POINT ( 'NONE',  ( 25.00000000000001421, 80.85786437626907741, 8.071067811865434649 ) ) ;
#4579=FACE_OUTER_BOUND ( 'NONE', #3701, .T. ) ;
#4581=ORIENTED_EDGE ( 'NONE', *, *, #5177, .F. ) ;
#4591=CARTESIAN_POINT ( 'NONE',  ( 25.00000000000000711, 40.21320343559642652, 10.99999999999999467 ) ) ;
#4601=CIRCLE ( 'NONE', #3740, 4.999999999999999112 ) ;
#4616=FACE_OUTER_BOUND ( 'NONE', #4010, .T. ) ;
#4628=DIRECTION ( 'NONE',  ( 0.000000000000000000, 0.000000000000000000, 1.000000000000000000 ) ) ;
#4649=LINE ( 'NONE', #4723, #6579 ) ;
#4662=EDGE_LOOP ( 'NONE', ( #6735, #5541, #356, #1727 ) ) ;
#4680=ORIENTED_EDGE ( 'NONE', *, *, #2073, .F. ) ;
#4681=CARTESIAN_POINT ( 'NONE',  ( 25.00000000000000000, 31.53553390593274841, 6.464466094067257806 ) ) ;
#4682=CARTESIAN_POINT ( 'NONE',  ( 1.387778780781445676E-14, 33.14213562373091548, 8.071067811865429320 ) ) ;
#4685=DIRECTION ( 'NONE',  ( -1.000000000000000000, 5.551115123125783935E-17, -4.237045877651919561E-33 ) ) ;
#4700=ORIENTED_EDGE ( 'NONE', *, *, #3053, .T. ) ;
#4720=AXIS2_PLACEMENT_3D ( 'NONE', #508, #6441, #664 ) ;
#4721=FACE_OUTER_BOUND ( 'NONE', #569, .T. ) ;
#4723=CARTESIAN_POINT ( 'NONE',  ( 25.00000000000000711, 40.21320343559642652, 5.999999999999996447 ) ) ;
#4731=FACE_OUTER_BOUND ( 'NONE', #949, .T. ) ;
#4739=ORIENTED_EDGE ( 'NONE', *, *, #7327, .F. ) ;
#4740=AXIS2_PLACEMENT_3D ( 'NONE', #526, #6346, #5228 ) ;
#4747=VERTEX_POINT ( 'NONE', #6436 ) ;
#4753=ORIENTED_EDGE ( 'NONE', *, *, #4532, .T. ) ;
#4757=PRODUCT_CONTEXT ( 'NONE', #4036, 'mechanical' ) ;
#4759=CYLINDRICAL_SURFACE ( 'NONE', #45, 4.999999999999999112 ) ;
#4766=CARTESIAN_POINT ( 'NONE',  ( 12.50000000000000355, 101.5000000000000000, -1.214306433183764966E-14 ) ) ;
#4775=DIRECTION ( 'NONE',  ( 5.551115123125782702E-17, 1.000000000000000000, 0.000000000000000000 ) ) ;
#4778=ORIENTED_EDGE ( 'NONE', *, *, #20, .T. ) ;
#4782=ORIENTED_EDGE ( 'NONE', *, *, #7568, .F. ) ;
#4812=ORIENTED_EDGE ( 'NONE', *, *, #4951, .T. ) ;
#4820=ORIENTED_EDGE ( 'NONE', *, *, #6731, .T. ) ;
#4823=VECTOR ( 'NONE', #4990, 1000.000000000000000 ) ;
#4832=EDGE_CURVE ( 'NONE', #2722, #5727, #5701, .T. ) ;
#4842=CARTESIAN_POINT ( 'NONE',  ( 0.000000000000000000, 78.92893218813448186, 2.928932188134520498 ) ) ;
#4843=LINE ( 'NONE', #5913, #68 ) ;
#4854=DIRECTION ( 'NONE',  ( 1.000000000000000000, -1.804112415015879773E-15, 4.237045877651875086E-33 ) ) ;
#4857=ORIENTED_EDGE ( 'NONE', *, *, #3053, .F. ) ;
#4867=AXIS2_PLACEMENT_3D ( 'NONE', #2655, #6811, #7348 ) ;
#4878=EDGE_CURVE ( 'NONE', #1964, #5278, #1119, .T. ) ;
#4894=ORIENTED_EDGE ( 'NONE', *, *, #2073, .T. ) ;
#4896=ORIENTED_EDGE ( 'NONE', *, *, #581, .F. ) ;
#4898=DIRECTION ( 'NONE',  ( 4.622231866529368100E-33, -2.600005424922769496E-32, 1.000000000000000000 ) ) ;
#4902=CARTESIAN_POINT ( 'NONE',  ( 24.99999999999999289, 86.00000000000001421, 9.999999999999992895 ) ) ;
#4905=CARTESIAN_POINT ( 'NONE',  ( 18.50000000000000711, 101.5000000000000000, 4.999999999999999112 ) ) ;
#4913=CARTESIAN_POINT ( 'NONE',  ( 25.00000000000000711, 28.00000000000002487, 9.999999999999996447 ) ) ;
#4916=DIRECTION ( 'NONE',  ( -1.000000000000000000, 5.551115123125783935E-17, -4.237045877651919561E-33 ) ) ;
#4917=EDGE_CURVE ( 'NONE', #5074, #6069, #4601, .T. ) ;
#4920=LINE ( 'NONE', #7258, #3577 ) ;
#4935=ORIENTED_EDGE ( 'NONE', *, *, #2870, .F. ) ;
#4947=AXIS2_PLACEMENT_3D ( 'NONE', #1453, #6730, #954 ) ;
#4951=EDGE_CURVE ( 'NONE', #4160, #1940, #413, .T. ) ;
#4960=ORIENTED_EDGE ( 'NONE', *, *, #1434, .F. ) ;
#4969=ORIENTED_EDGE ( 'NONE', *, *, #1905, .F. ) ;
#4982=CARTESIAN_POINT ( 'NONE',  ( 24.99999999999999289, 86.00000000000001421, 4.999999999999992006 ) ) ;
#4988=ORIENTED_EDGE ( 'NONE', *, *, #5736, .F. ) ;
#4989=( NAMED_UNIT ( * ) SI_UNIT ( $, .STERADIAN. ) SOLID_ANGLE_UNIT ( ) );
#4990=DIRECTION ( 'NONE',  ( -1.000000000000000000, 5.551115123125783935E-17, -4.237045877651919561E-33 ) ) ;
#4991=CARTESIAN_POINT ( 'NONE',  ( 25.00000000000000711, 40.21320343559642652, 5.999999999999996447 ) ) ;
#5001=CARTESIAN_POINT ( 'NONE',  ( 25.00000000000000711, 77.32233047033632545, 4.535533905932710219 ) ) ;
#5003=EDGE_CURVE ( 'NONE', #5285, #5929, #1852, .T. ) ;
#5010=EDGE_LOOP ( 'NONE', ( #1322, #4739, #3869, #6380 ) ) ;
#5014=ORIENTED_EDGE ( 'NONE', *, *, #993, .F. ) ;
#5032=EDGE_LOOP ( 'NONE', ( #2289, #2068 ) ) ;
#5042=VECTOR ( 'NONE', #116, 999.9999999999998863 ) ;
#5051=ORIENTED_EDGE ( 'NONE', *, *, #7577, .F. ) ;
#5060=( NAMED_UNIT ( * ) SI_UNIT ( $, .STERADIAN. ) SOLID_ANGLE_UNIT ( ) );
#5073=CYLINDRICAL_SURFACE ( 'NONE', #760, 9.999999999999996447 ) ;
#5074=VERTEX_POINT ( 'NONE', #6118 ) ;
#5081=CYLINDRICAL_SURFACE ( 'NONE', #4867, 6.000000000000001776 ) ;
#5100=ADVANCED_BREP_SHAPE_REPRESENTATION ( '', ( #6388, #1914 ), #7073 ) ;
#5114=ORIENTED_EDGE ( 'NONE', *, *, #2636, .F. ) ;
#5119=LINE ( 'NONE', #6917, #1128 ) ;
#5121=EDGE_LOOP ( 'NONE', ( #3710, #972, #5997, #4820 ) ) ;
#5140=CARTESIAN_POINT ( 'NONE',  ( 25.00000000000002132, 28.00000000000002487, 0.000000000000000000 ) ) ;
#5144=DIRECTION ( 'NONE',  ( 4.622231866529368100E-33, -2.600005424922769496E-32, 1.000000000000000000 ) ) ;
#5154=VERTEX_POINT ( 'NONE', #3234 ) ;
#5159=CARTESIAN_POINT ( 'NONE',  ( 12.50000000000000355, 101.5000000000000000, 4.999999999999999112 ) ) ;
#5170=DIRECTION ( 'NONE',  ( 0.000000000000000000, 0.000000000000000000, 1.000000000000000000 ) ) ;
#5173=ORIENTED_EDGE ( 'NONE', *, *, #3395, .T. ) ;
#5177=EDGE_CURVE ( 'NONE', #6636, #2714, #3007, .T. ) ;
#5197=LINE ( 'NONE', #1039, #5915 ) ;
#5198=DIRECTION ( 'NONE',  ( 1.000000000000000000, -5.551115123125783935E-17, 4.237045877651919561E-33 ) ) ;
#5204=ORIENTED_EDGE ( 'NONE', *, *, #2200, .T. ) ;
#5214=CIRCLE ( 'NONE', #2628, 9.999999999999994671 ) ;
#5215=DIRECTION ( 'NONE',  ( 0.000000000000000000, 0.000000000000000000, 1.000000000000000000 ) ) ;
#5217=CARTESIAN_POINT ( 'NONE',  ( 2.775557561562891351E-14, 86.00000000000000000, 9.999999999999996447 ) ) ;
#5219=CARTESIAN_POINT ( 'NONE',  ( 12.50000000000001066, 12.50000000000001066, -1.214306433183764966E-14 ) ) ;
#5225=CARTESIAN_POINT ( 'NONE',  ( 1.387778780781445676E-14, 31.53553390593269512, 6.464466094067257806 ) ) ;
#5228=DIRECTION ( 'NONE',  ( 1.000000000000000000, 0.000000000000000000, 0.000000000000000000 ) ) ;
#5236=DIRECTION ( 'NONE',  ( -1.000000000000000000, 0.000000000000000000, -4.237045877651919561E-33 ) ) ;
#5242=VECTOR ( 'NONE', #3661, 1000.000000000000000 ) ;
#5250=AXIS2_PLACEMENT_3D ( 'NONE', #4913, #4487, #4333 ) ;
#5255=CARTESIAN_POINT ( 'NONE',  ( 0.000000000000000000, 35.07106781186547551, 2.928932188134525827 ) ) ;
#5263=EDGE_CURVE ( 'NONE', #6977, #5737, #1033, .T. ) ;
#5277=FACE_OUTER_BOUND ( 'NONE', #4662, .T. ) ;
#5278=VERTEX_POINT ( 'NONE', #3927 ) ;
#5280=DIRECTION ( 'NONE',  ( 0.000000000000000000, 0.000000000000000000, 1.000000000000000000 ) ) ;
#5285=VERTEX_POINT ( 'NONE', #5740 ) ;
#5287=CIRCLE ( 'NONE', #1467, 10.00000000000000711 ) ;
#5295=AXIS2_PLACEMENT_3D ( 'NONE', #2819, #2206, #5170 ) ;
#5301=DIRECTION ( 'NONE',  ( 5.551115123125783935E-17, 1.000000000000000000, 5.166928274020107347E-17 ) ) ;
#5303=VERTEX_POINT ( 'NONE', #6390 ) ;
#5311=CARTESIAN_POINT ( 'NONE',  ( 25.00000000000000000, 31.53553390593274841, 6.464466094067261359 ) ) ;
#5333=ORIENTED_EDGE ( 'NONE', *, *, #5809, .T. ) ;
#5348=ORIENTED_EDGE ( 'NONE', *, *, #2725, .F. ) ;
#5350=AXIS2_PLACEMENT_3D ( 'NONE', #2404, #514, #5215 ) ;
#5355=VERTEX_POINT ( 'NONE', #7533 ) ;
#5383=CARTESIAN_POINT ( 'NONE',  ( 25.00000000000000000, 31.53553390593274841, 6.464466094067261359 ) ) ;
#5384=AXIS2_PLACEMENT_3D ( 'NONE', #1185, #1111, #5236 ) ;
#5388=CARTESIAN_POINT ( 'NONE',  ( 25.00000000000002132, 73.78679656440357348, 0.9999999999999991118 ) ) ;
#5390=ORIENTED_EDGE ( 'NONE', *, *, #1977, .F. ) ;
#5410=CARTESIAN_POINT ( 'NONE',  ( 25.00000000000000000, 40.21320343559644783, 5.999999999999996447 ) ) ;
#5434=VECTOR ( 'NONE', #6056, 1000.000000000000000 ) ;
#5436=CARTESIAN_POINT ( 'NONE',  ( 25.00000000000002842, 73.78679656440351664, 11.00000000000000178 ) ) ;
#5443=DIRECTION ( 'NONE',  ( 0.000000000000000000, 0.000000000000000000, 1.000000000000000000 ) ) ;
#5458=CIRCLE ( 'NONE', #2130, 5.000000000000004441 ) ;
#5469=EDGE_CURVE ( 'NONE', #2726, #3811, #3628, .T. ) ;
#5476=CARTESIAN_POINT ( 'NONE',  ( 24.99999999999998579, 101.4999999999999858, 9.999999999999996447 ) ) ;
#5491=DIRECTION ( 'NONE',  ( -1.000000000000000000, 5.551115123125783935E-17, -4.237045877651919561E-33 ) ) ;
#5493=FACE_BOUND ( 'NONE', #6525, .T. ) ;
#5538=CYLINDRICAL_SURFACE ( 'NONE', #4947, 6.000000000000001776 ) ;
#5541=ORIENTED_EDGE ( 'NONE', *, *, #6731, .F. ) ;
#5545=DIRECTION ( 'NONE',  ( 1.000000000000000000, 2.220446049250313870E-15, 4.237045877651953088E-33 ) ) ;
#5548=CARTESIAN_POINT ( 'NONE',  ( 25.00000000000002132, 36.67766952966366745, 4.535533905932717325 ) ) ;
#5549=CARTESIAN_POINT ( 'NONE',  ( 25.00000000000000711, 28.00000000000002487, 9.999999999999996447 ) ) ;
#5596=DIRECTION ( 'NONE',  ( 1.000000000000000000, 0.000000000000000000, 0.000000000000000000 ) ) ;
#5598=VERTEX_POINT ( 'NONE', #2036 ) ;
#5604=FACE_OUTER_BOUND ( 'NONE', #3956, .T. ) ;
#5606=LINE ( 'NONE', #5140, #3629 ) ;
#5611=VERTEX_POINT ( 'NONE', #3771 ) ;
#5616=FACE_OUTER_BOUND ( 'NONE', #6558, .T. ) ;
#5617=ORIENTED_EDGE ( 'NONE', *, *, #4429, .T. ) ;
#5675=DIRECTION ( 'NONE',  ( -6.162975822039153361E-33, -5.166928274020107963E-17, 1.000000000000000000 ) ) ;
#5689=CARTESIAN_POINT ( 'NONE',  ( 25.00000000000001421, 80.85786437626907741, 8.071067811865434649 ) ) ;
#5700=EDGE_LOOP ( 'NONE', ( #2153, #468, #5348, #4935 ) ) ;
#5701=CIRCLE ( 'NONE', #1515, 4.999999999999999112 ) ;
#5702=CIRCLE ( 'NONE', #3741, 5.000000000000004441 ) ;
#5709=VECTOR ( 'NONE', #4898, 1000.000000000000000 ) ;
#5711=ORIENTED_EDGE ( 'NONE', *, *, #6993, .F. ) ;
#5721=LINE ( 'NONE', #365, #251 ) ;
#5727=VERTEX_POINT ( 'NONE', #6221 ) ;
#5734=VECTOR ( 'NONE', #3111, 1000.000000000000114 ) ;
#5736=EDGE_CURVE ( 'NONE', #868, #5355, #306, .T. ) ;
#5737=VERTEX_POINT ( 'NONE', #5689 ) ;
#5740=CARTESIAN_POINT ( 'NONE',  ( 25.00000000000000000, 12.49999999999998401, 4.999999999999995559 ) ) ;
#5760=PLANE ( 'NONE',  #3691 ) ;
#5773=ADVANCED_FACE ( 'NONE', ( #2148 ), #4503, .T. ) ;
#5782=DIRECTION ( 'NONE',  ( -1.000000000000000000, 5.551115123125783935E-17, -4.237045877651919561E-33 ) ) ;
#5801=EDGE_LOOP ( 'NONE', ( #4087, #4526, #4812, #2006 ) ) ;
#5809=EDGE_CURVE ( 'NONE', #3515, #2618, #5702, .T. ) ;
#5810=ORIENTED_EDGE ( 'NONE', *, *, #2708, .T. ) ;
#5845=DIRECTION ( 'NONE',  ( 1.000000000000000000, -5.551115123125783935E-17, 4.237045877651919561E-33 ) ) ;
#5849=ORIENTED_EDGE ( 'NONE', *, *, #7107, .T. ) ;
#5852=CYLINDRICAL_SURFACE ( 'NONE', #5384, 12.49999999999999467 ) ;
#5868=ORIENTED_EDGE ( 'NONE', *, *, #6620, .T. ) ;
#5874=LINE ( 'NONE', #5410, #2825 ) ;
#5882=EDGE_LOOP ( 'NONE', ( #3551, #2855, #2918, #4053 ) ) ;
#5891=ORIENTED_EDGE ( 'NONE', *, *, #2725, .T. ) ;
#5897=CARTESIAN_POINT ( 'NONE',  ( 1.387778780781445676E-14, 101.5000000000000000, 4.999999999999999112 ) ) ;
#5900=EDGE_CURVE ( 'NONE', #4443, #2926, #6925, .T. ) ;
#5912=DIRECTION ( 'NONE',  ( 5.551115123125783935E-17, 0.7071067811865499042, 0.7071067811865451302 ) ) ;
#5913=CARTESIAN_POINT ( 'NONE',  ( 24.99999999999999289, 86.00000000000001421, 4.999999999999992006 ) ) ;
#5915=VECTOR ( 'NONE', #7536, 1000.000000000000000 ) ;
#5921=LINE ( 'NONE', #648, #457 ) ;
#5924=ORIENTED_EDGE ( 'NONE', *, *, #1396, .T. ) ;
#5929=VERTEX_POINT ( 'NONE', #7111 ) ;
#5939=DIRECTION ( 'NONE',  ( -1.000000000000000000, 5.551115123125783935E-17, -4.237045877651919561E-33 ) ) ;
#5955=EDGE_CURVE ( 'NONE', #5154, #1377, #2742, .T. ) ;
#5971=EDGE_LOOP ( 'NONE', ( #3619, #1358 ) ) ;
#5972=DIRECTION ( 'NONE',  ( 4.622231866529368100E-33, -2.600005424922769496E-32, 1.000000000000000000 ) ) ;
#5981=PRODUCT_DEFINITION ( 'UNKNOWN', '', #6089, #1794 ) ;
#5985=CARTESIAN_POINT ( 'NONE',  ( 25.00000000000000000, 73.78679656440354506, 5.999999999999996447 ) ) ;
#5997=ORIENTED_EDGE ( 'NONE', *, *, #1434, .T. ) ;
#6002=CARTESIAN_POINT ( 'NONE',  ( 12.50000000000001066, 12.50000000000001066, 0.000000000000000000 ) ) ;
#6022=UNCERTAINTY_MEASURE_WITH_UNIT (LENGTH_MEASURE( 1.000000000000000082E-05 ), #214, 'distance_accuracy_value', 'NONE');
#6027=EDGE_CURVE ( 'NONE', #6493, #5278, #659, .T. ) ;
#6043=ADVANCED_FACE ( 'NONE', ( #7060 ), #1750, .F. ) ;
#6046=CARTESIAN_POINT ( 'NONE',  ( 12.50000000000000355, 101.5000000000000000, 4.999999999999999112 ) ) ;
#6056=DIRECTION ( 'NONE',  ( 4.622231866529368100E-33, -2.600005424922769496E-32, 1.000000000000000000 ) ) ;
#6059=ADVANCED_FACE ( 'NONE', ( #2940 ), #6452, .F. ) ;
#6064=DIRECTION ( 'NONE',  ( 1.000000000000000000, -5.551115123125783935E-17, 4.237045877651919561E-33 ) ) ;
#6069=VERTEX_POINT ( 'NONE', #1100 ) ;
#6076=CARTESIAN_POINT ( 'NONE',  ( 6.500000000000002665, 101.5000000000000000, -1.214306433183764966E-14 ) ) ;
#6085=ORIENTED_EDGE ( 'NONE', *, *, #1949, .F. ) ;
#6089=PRODUCT_DEFINITION_FORMATION_WITH_SPECIFIED_SOURCE ( 'ANY', '', #3210, .NOT_KNOWN. ) ;
#6097=FACE_OUTER_BOUND ( 'NONE', #4418, .T. ) ;
#6100=PLANE ( 'NONE',  #6107 ) ;
#6103=LINE ( 'NONE', #1403, #553 ) ;
#6106=DIRECTION ( 'NONE',  ( 4.622231866529368100E-33, -2.600005424922769496E-32, 1.000000000000000000 ) ) ;
#6107=AXIS2_PLACEMENT_3D ( 'NONE', #6134, #6209, #860 ) ;
#6110=LINE ( 'NONE', #6580, #5242 ) ;
#6118=CARTESIAN_POINT ( 'NONE',  ( 2.775557561562891351E-14, 36.67766952966363903, 4.535533905932717325 ) ) ;
#6134=CARTESIAN_POINT ( 'NONE',  ( 24.99999999999999289, 86.00000000000001421, 4.999999999999992006 ) ) ;
#6143=CARTESIAN_POINT ( 'NONE',  ( 3.469446951953614189E-14, 80.85786437626907741, 8.071067811865438202 ) ) ;
#6161=VECTOR ( 'NONE', #802, 1000.000000000000000 ) ;
#6181=ORIENTED_EDGE ( 'NONE', *, *, #4117, .T. ) ;
#6209=DIRECTION ( 'NONE',  ( -4.237045877651920929E-33, -2.600005424922769496E-32, 1.000000000000000000 ) ) ;
#6221=CARTESIAN_POINT ( 'NONE',  ( 25.00000000000000711, 77.32233047033632545, 4.535533905932710219 ) ) ;
#6228=CIRCLE ( 'NONE', #2051, 9.999999999999996447 ) ;
#6238=ORIENTED_EDGE ( 'NONE', *, *, #5177, .T. ) ;
#6260=DIRECTION ( 'NONE',  ( -1.000000000000000000, 5.551115123125783935E-17, -4.237045877651919561E-33 ) ) ;
#6262=VERTEX_POINT ( 'NONE', #5225 ) ;
#6274=AXIS2_PLACEMENT_3D ( 'NONE', #7347, #1533, #3817 ) ;
#6290=DIRECTION ( 'NONE',  ( 1.000000000000000000, 0.000000000000000000, 0.000000000000000000 ) ) ;
#6293=EDGE_CURVE ( 'NONE', #452, #2583, #5214, .T. ) ;
#6306=ORIENTED_EDGE ( 'NONE', *, *, #4878, .T. ) ;
#6326=CARTESIAN_POINT ( 'NONE',  ( 12.50000000000001066, 12.50000000000001066, 4.999999999999995559 ) ) ;
#6337=CARTESIAN_POINT ( 'NONE',  ( 12.50000000000001066, 12.50000000000001066, -1.214306433183764966E-14 ) ) ;
#6345=DIRECTION ( 'NONE',  ( 7.318533788671501715E-33, 1.945189243831109580E-32, -1.000000000000000000 ) ) ;
#6346=DIRECTION ( 'NONE',  ( 4.622231866529368100E-33, -2.600005424922769496E-32, 1.000000000000000000 ) ) ;
#6350=ORIENTED_EDGE ( 'NONE', *, *, #1905, .T. ) ;
#6377=DIRECTION ( 'NONE',  ( 1.000000000000000000, -5.551115123125783935E-17, 4.237045877651919561E-33 ) ) ;
#6380=ORIENTED_EDGE ( 'NONE', *, *, #7337, .T. ) ;
#6382=CARTESIAN_POINT ( 'NONE',  ( 25.00000000000000711, 40.21320343559642652, 0.9999999999999956701 ) ) ;
#6388=MANIFOLD_SOLID_BREP ( 'Cut-Extrude1', #134 ) ;
#6390=CARTESIAN_POINT ( 'NONE',  ( 2.775557561562891351E-14, 28.00000000000002487, 4.999999999999995559 ) ) ;
#6405=EDGE_CURVE ( 'NONE', #4443, #4747, #5606, .T. ) ;
#6410=DIRECTION ( 'NONE',  ( 5.551115123125785167E-17, -0.7071067811865451302, 0.7071067811865499042 ) ) ;
#6423=AXIS2_PLACEMENT_3D ( 'NONE', #7243, #1902, #7284 ) ;
#6427=DIRECTION ( 'NONE',  ( -1.000000000000000000, 5.551115123125783935E-17, -4.237045877651919561E-33 ) ) ;
#6430=CARTESIAN_POINT ( 'NONE',  ( 25.00000000000002842, 33.14213562373094391, 8.071067811865434649 ) ) ;
#6436=CARTESIAN_POINT ( 'NONE',  ( 2.775557561562891351E-14, 28.00000000000002487, -1.734723475976807094E-15 ) ) ;
#6441=DIRECTION ( 'NONE',  ( 1.000000000000000000, -5.551115123125783935E-17, 4.237045877651919561E-33 ) ) ;
#6448=EDGE_CURVE ( 'NONE', #1494, #2116, #1283, .T. ) ;
#6452=PLANE ( 'NONE',  #897 ) ;
#6458=EDGE_CURVE ( 'NONE', #1663, #1964, #3389, .T. ) ;
#6475=SHAPE_REPRESENTATION ( 'link', ( #1914 ), #7073 ) ;
#6477=DIRECTION ( 'NONE',  ( 5.551115123125783935E-17, 1.000000000000000000, -2.214819436045321778E-32 ) ) ;
#6484=VECTOR ( 'NONE', #2235, 1000.000000000000000 ) ;
#6493=VERTEX_POINT ( 'NONE', #4682 ) ;
#6511=ORIENTED_EDGE ( 'NONE', *, *, #5955, .F. ) ;
#6520=EDGE_LOOP ( 'NONE', ( #235, #5390, #1810, #2057 ) ) ;
#6524=FACE_OUTER_BOUND ( 'NONE', #3093, .T. ) ;
#6525=EDGE_LOOP ( 'NONE', ( #4581, #6774 ) ) ;
#6558=EDGE_LOOP ( 'NONE', ( #4026, #5173, #5924, #4969 ) ) ;
#6559=DIRECTION ( 'NONE',  ( -1.000000000000000000, 5.551115123125783935E-17, -4.237045877651919561E-33 ) ) ;
#6564=ADVANCED_FACE ( 'NONE', ( #6524 ), #3602, .F. ) ;
#6579=VECTOR ( 'NONE', #7592, 1000.000000000000000 ) ;
#6580=CARTESIAN_POINT ( 'NONE',  ( 1.387778780781445676E-14, 40.21320343559642652, 5.999999999999996447 ) ) ;
#6601=DIRECTION ( 'NONE',  ( 5.551115123125783935E-17, 1.000000000000000000, -2.214819436045321778E-32 ) ) ;
#6620=EDGE_CURVE ( 'NONE', #4037, #6725, #2518, .T. ) ;
#6626=CYLINDRICAL_SURFACE ( 'NONE', #1656, 10.00000000000000711 ) ;
#6627=ORIENTED_EDGE ( 'NONE', *, *, #581, .T. ) ;
#6636=VERTEX_POINT ( 'NONE', #2474 ) ;
#6642=CARTESIAN_POINT ( 'NONE',  ( 24.99999999999999289, 86.00000000000001421, -1.214306433183764966E-14 ) ) ;
#6645=VECTOR ( 'NONE', #3409, 1000.000000000000000 ) ;
#6646=ORIENTED_EDGE ( 'NONE', *, *, #7076, .F. ) ;
#6660=LINE ( 'NONE', #4431, #3952 ) ;
#6672=ORIENTED_EDGE ( 'NONE', *, *, #3422, .T. ) ;
#6677=CARTESIAN_POINT ( 'NONE',  ( 25.00000000000000711, 77.32233047033632545, 4.535533905932713772 ) ) ;
#6680=ORIENTED_EDGE ( 'NONE', *, *, #3745, .T. ) ;
#6693=ORIENTED_EDGE ( 'NONE', *, *, #6405, .F. ) ;
#6702=FACE_OUTER_BOUND ( 'NONE', #1301, .T. ) ;
#6725=VERTEX_POINT ( 'NONE', #7170 ) ;
#6730=DIRECTION ( 'NONE',  ( 4.622231866529368100E-33, -2.600005424922769496E-32, 1.000000000000000000 ) ) ;
#6731=EDGE_CURVE ( 'NONE', #1595, #6262, #4325, .T. ) ;
#6733=ORIENTED_EDGE ( 'NONE', *, *, #5469, .F. ) ;
#6735=ORIENTED_EDGE ( 'NONE', *, *, #893, .F. ) ;
#6746=LINE ( 'NONE', #287, #135 ) ;
#6757=ORIENTED_EDGE ( 'NONE', *, *, #7481, .T. ) ;
#6774=ORIENTED_EDGE ( 'NONE', *, *, #1396, .F. ) ;
#6786=ORIENTED_EDGE ( 'NONE', *, *, #7135, .T. ) ;
#6790=PLANE ( 'NONE',  #7267 ) ;
#6811=DIRECTION ( 'NONE',  ( 4.622231866529368100E-33, -2.600005424922769496E-32, 1.000000000000000000 ) ) ;
#6829=DIRECTION ( 'NONE',  ( -1.000000000000000000, 5.551115123125783935E-17, -4.237045877651919561E-33 ) ) ;
#6832=DIRECTION ( 'NONE',  ( 0.000000000000000000, 0.000000000000000000, -1.000000000000000000 ) ) ;
#6835=ORIENTED_EDGE ( 'NONE', *, *, #4324, .F. ) ;
#6851=ORIENTED_EDGE ( 'NONE', *, *, #5263, .F. ) ;
#6866=EDGE_CURVE ( 'NONE', #1940, #4160, #420, .T. ) ;
#6869=DIRECTION ( 'NONE',  ( 5.551115123125783935E-17, 1.000000000000000000, 5.166928274020107347E-17 ) ) ;
#6878=CARTESIAN_POINT ( 'NONE',  ( 12.50000000000001066, 12.50000000000001066, 4.999999999999995559 ) ) ;
#6917=CARTESIAN_POINT ( 'NONE',  ( 2.775557561562891351E-14, 86.00000000000000000, -1.734723475976807094E-15 ) ) ;
#6923=CIRCLE ( 'NONE', #2986, 12.49999999999999645 ) ;
#6925=CIRCLE ( 'NONE', #4348, 9.999999999999996447 ) ;
#6933=EDGE_CURVE ( 'NONE', #7420, #5303, #1120, .T. ) ;
#6939=LINE ( 'NONE', #1703, #6645 ) ;
#6952=DIRECTION ( 'NONE',  ( -4.237045877651920929E-33, -2.600005424922769496E-32, 1.000000000000000000 ) ) ;
#6958=CARTESIAN_POINT ( 'NONE',  ( 12.50000000000001066, 12.50000000000001066, -1.214306433183764966E-14 ) ) ;
#6973=AXIS2_PLACEMENT_3D ( 'NONE', #2473, #2977, #707 ) ;
#6977=VERTEX_POINT ( 'NONE', #5436 ) ;
#6993=EDGE_CURVE ( 'NONE', #5598, #2040, #1344, .T. ) ;
#6999=CIRCLE ( 'NONE', #248, 6.000000000000001776 ) ;
#7021=PLANE ( 'NONE',  #1528 ) ;
#7022=DIRECTION ( 'NONE',  ( 5.551115123125786400E-17, 1.000000000000000000, -3.556183125752453755E-15 ) ) ;
#7028=ORIENTED_EDGE ( 'NONE', *, *, #2137, .T. ) ;
#7032=DIRECTION ( 'NONE',  ( 1.000000000000000000, -5.551115123125783935E-17, 4.237045877651919561E-33 ) ) ;
#7033=CARTESIAN_POINT ( 'NONE',  ( 1.387778780781445676E-14, 40.21320343559642652, 10.99999999999999467 ) ) ;
#7049=FACE_OUTER_BOUND ( 'NONE', #3087, .T. ) ;
#7050=DIRECTION ( 'NONE',  ( 4.622231866529368100E-33, -2.600005424922769496E-32, 1.000000000000000000 ) ) ;
#7054=DIRECTION ( 'NONE',  ( -5.551115123125785167E-17, 0.7071067811865469066, 0.7071067811865482389 ) ) ;
#7060=FACE_OUTER_BOUND ( 'NONE', #2632, .T. ) ;
#7065=VECTOR ( 'NONE', #3072, 1000.000000000000000 ) ;
#7073=( GEOMETRIC_REPRESENTATION_CONTEXT ( 3 ) GLOBAL_UNCERTAINTY_ASSIGNED_CONTEXT ( ( #6022 ) ) GLOBAL_UNIT_ASSIGNED_CONTEXT ( ( #214, #7212, #4989 ) ) REPRESENTATION_CONTEXT ( 'NONE', 'WORKASPACE' ) );
#7076=EDGE_CURVE ( 'NONE', #6725, #5598, #178, .T. ) ;
#7080=CARTESIAN_POINT ( 'NONE',  ( 24.99999999999999289, 86.00000000000001421, 9.999999999999992895 ) ) ;
#7095=PRODUCT_DEFINITION_SHAPE ( 'NONE', 'NONE',  #5981 ) ;
#7099=CYLINDRICAL_SURFACE ( 'NONE', #2794, 9.999999999999996447 ) ;
#7101=CARTESIAN_POINT ( 'NONE',  ( 2.775557561562891351E-14, 40.21320343559642652, 0.9999999999999956701 ) ) ;
#7107=EDGE_CURVE ( 'NONE', #7449, #5598, #7564, .T. ) ;
#7111=CARTESIAN_POINT ( 'NONE',  ( 25.00000000000000711, 28.00000000000002487, 4.999999999999995559 ) ) ;
#7116=PLANE ( 'NONE',  #4143 ) ;
#7126=SHAPE_DEFINITION_REPRESENTATION ( #7095, #6475 ) ;
#7134=FACE_OUTER_BOUND ( 'NONE', #7308, .T. ) ;
#7135=EDGE_CURVE ( 'NONE', #5727, #5611, #1717, .T. ) ;
#7168=EDGE_CURVE ( 'NONE', #5737, #2583, #2188, .T. ) ;
#7170=CARTESIAN_POINT ( 'NONE',  ( 1.387778780781445676E-14, 101.5000000000000000, -1.734723475976807094E-15 ) ) ;
#7171=PLANE ( 'NONE',  #6423 ) ;
#7179=DIRECTION ( 'NONE',  ( -1.000000000000000000, 5.551115123125783935E-17, -4.237045877651919561E-33 ) ) ;
#7185=ORIENTED_EDGE ( 'NONE', *, *, #6293, .T. ) ;
#7191=FACE_BOUND ( 'NONE', #728, .T. ) ;
#7199=DIRECTION ( 'NONE',  ( 1.000000000000000000, 0.000000000000000000, 0.000000000000000000 ) ) ;
#7212=( NAMED_UNIT ( * ) PLANE_ANGLE_UNIT ( ) SI_UNIT ( $, .RADIAN. ) );
#7218=CARTESIAN_POINT ( 'NONE',  ( 1.387778780781445676E-14, 77.32233047033629703, 4.535533905932711995 ) ) ;
#7228=EDGE_CURVE ( 'NONE', #3811, #2618, #4843, .T. ) ;
#7243=CARTESIAN_POINT ( 'NONE',  ( 25.00000000000000000, 40.21320343559644783, 10.99999999999999467 ) ) ;
#7255=PLANE ( 'NONE',  #4121 ) ;
#7258=CARTESIAN_POINT ( 'NONE',  ( 6.500000000000009770, 12.50000000000001243, -1.214306433183764966E-14 ) ) ;
#7267=AXIS2_PLACEMENT_3D ( 'NONE', #1510, #5675, #2744 ) ;
#7282=EDGE_LOOP ( 'NONE', ( #4181, #3965, #1795, #6693 ) ) ;
#7284=DIRECTION ( 'NONE',  ( -5.551115123125783935E-17, -1.000000000000000000, -5.166928274020107963E-17 ) ) ;
#7285=CARTESIAN_POINT ( 'NONE',  ( 6.938893903907228378E-15, 73.78679656440351664, 10.99999999999999467 ) ) ;
#7303=AXIS2_PLACEMENT_3D ( 'NONE', #4180, #5939, #1129 ) ;
#7308=EDGE_LOOP ( 'NONE', ( #4056, #1621, #5204, #6627 ) ) ;
#7319=DIRECTION ( 'NONE',  ( 5.551115123125783935E-17, 1.000000000000000000, -2.214819436045321778E-32 ) ) ;
#7327=EDGE_CURVE ( 'NONE', #908, #5074, #7598, .T. ) ;
#7330=CIRCLE ( 'NONE', #4024, 6.000000000000001776 ) ;
#7337=EDGE_CURVE ( 'NONE', #2926, #2183, #3800, .T. ) ;
#7347=CARTESIAN_POINT ( 'NONE',  ( 25.00000000000001421, 35.07106781186547551, 2.928932188134525827 ) ) ;
#7348=DIRECTION ( 'NONE',  ( 1.000000000000000000, 0.000000000000000000, 0.000000000000000000 ) ) ;
#7350=LINE ( 'NONE', #7495, #6484 ) ;
#7363=LINE ( 'NONE', #3216, #2967 ) ;
#7376=ADVANCED_FACE ( 'NONE', ( #5493, #3726 ), #7255, .T. ) ;
#7395=ORIENTED_EDGE ( 'NONE', *, *, #20, .F. ) ;
#7406=CIRCLE ( 'NONE', #2746, 6.000000000000001776 ) ;
#7407=ORIENTED_EDGE ( 'NONE', *, *, #1977, .T. ) ;
#7412=DIRECTION ( 'NONE',  ( 0.000000000000000000, 1.000000000000000000, -1.617781153285278938E-32 ) ) ;
#7420=VERTEX_POINT ( 'NONE', #2673 ) ;
#7428=VECTOR ( 'NONE', #1899, 1000.000000000000000 ) ;
#7429=VECTOR ( 'NONE', #4916, 1000.000000000000000 ) ;
#7431=EDGE_CURVE ( 'NONE', #5929, #5303, #6103, .T. ) ;
#7434=DIRECTION ( 'NONE',  ( 4.622231866529368100E-33, -2.600005424922769496E-32, 1.000000000000000000 ) ) ;
#7436=ORIENTED_EDGE ( 'NONE', *, *, #7135, .F. ) ;
#7449=VERTEX_POINT ( 'NONE', #6642 ) ;
#7464=DIRECTION ( 'NONE',  ( -1.000000000000000000, 5.551115123125783935E-17, -4.237045877651919561E-33 ) ) ;
#7481=EDGE_CURVE ( 'NONE', #5611, #2534, #4530, .T. ) ;
#7487=ORIENTED_EDGE ( 'NONE', *, *, #6458, .T. ) ;
#7495=CARTESIAN_POINT ( 'NONE',  ( 18.50000000000001421, 12.50000000000001066, -1.214306433183764966E-14 ) ) ;
#7502=ORIENTED_EDGE ( 'NONE', *, *, #3273, .F. ) ;
#7507=ORIENTED_EDGE ( 'NONE', *, *, #4832, .T. ) ;
#7530=ORIENTED_EDGE ( 'NONE', *, *, #6866, .T. ) ;
#7533=CARTESIAN_POINT ( 'NONE',  ( 6.500000000000000888, 101.5000000000000000, -1.214306433183764966E-14 ) ) ;
#7536=DIRECTION ( 'NONE',  ( 5.551115123125783935E-17, 1.000000000000000000, -2.214819436045321778E-32 ) ) ;
#7553=VECTOR ( 'NONE', #2024, 1000.000000000000000 ) ;
#7564=LINE ( 'NONE', #273, #3380 ) ;
#7568=EDGE_CURVE ( 'NONE', #2183, #5074, #4219, .T. ) ;
#7577=EDGE_CURVE ( 'NONE', #472, #6069, #4649, .T. ) ;
#7578=CARTESIAN_POINT ( 'NONE',  ( 25.00000000000002132, 0.000000000000000000, -1.734723475976807094E-15 ) ) ;
#7589=ADVANCED_FACE ( 'NONE', ( #7134 ), #7021, .T. ) ;
#7592=DIRECTION ( 'NONE',  ( -1.000000000000000000, 5.551115123125783935E-17, -4.237045877651919561E-33 ) ) ;
#7596=EDGE_LOOP ( 'NONE', ( #4700, #839, #4168, #5810 ) ) ;
#7598=LINE ( 'NONE', #1329, #7429 ) ;
#7618=COLOUR_RGB('Light Blue',0.38,0.62,0.78);
#7619=FILL_AREA_STYLE_COLOUR('',#7618);
#7620=FILL_AREA_STYLE('',(#7619));
#7621=SURFACE_STYLE_FILL_AREA(#7620);
#7622=SURFACE_SIDE_STYLE('',(#7621));
#7623=SURFACE_STYLE_USAGE(.BOTH.,#7622);
#7624=PRESENTATION_STYLE_ASSIGNMENT((#7623));
ENDSEC;
END-ISO-10303-21;
